ISO-10303-21;
HEADER;
/* Generated by software containing ST-Developer
 * from STEP Tools, Inc. (www.steptools.com) 
 */

FILE_DESCRIPTION(
/* description */ ('Turntable on roller ring'),
/* implementation_level */ '2;1');

FILE_NAME(
/* name */ 'Inner race spacer (1).step',
/* time_stamp */ '2026-10-28T03:23:59-07:00',
/* author */ (''),
/* organization */ (''),
/* preprocessor_version */ 'ST-DEVELOPER v20.2',
/* originating_system */ 'Autodesk Translation Framework v15.17.0.0',
/* authorisation */ '');

FILE_SCHEMA (('AUTOMOTIVE_DESIGN { 1 0 10303 214 3 1 1 }'));
ENDSEC;

DATA;
#10=MECHANICAL_DESIGN_GEOMETRIC_PRESENTATION_REPRESENTATION('',(#645),#16281);
#526=SHAPE_REPRESENTATION_RELATIONSHIP('SRR','None',#16543,#581);
#581=ADVANCED_BREP_SHAPE_REPRESENTATION('',(#715),#16237);
#645=STYLED_ITEM('',(#16932),#715);
#715=MANIFOLD_SOLID_BREP('Body1',#8388);
#885=FACE_BOUND('',#2129,.T.);
#886=FACE_BOUND('',#2131,.T.);
#1105=PLANE('',#9598);
#1106=PLANE('',#9599);
#1493=FACE_OUTER_BOUND('',#2126,.T.);
#1494=FACE_OUTER_BOUND('',#2127,.T.);
#1495=FACE_OUTER_BOUND('',#2128,.T.);
#1496=FACE_OUTER_BOUND('',#2130,.T.);
#2126=EDGE_LOOP('',(#6683,#6684,#6685,#6686));
#2127=EDGE_LOOP('',(#6687,#6688,#6689,#6690));
#2128=EDGE_LOOP('',(#6691));
#2129=EDGE_LOOP('',(#6692));
#2130=EDGE_LOOP('',(#6693));
#2131=EDGE_LOOP('',(#6694));
#2733=LINE('',#14605,#3216);
#2734=LINE('',#14611,#3217);
#3216=VECTOR('',#11548,0.505);
#3217=VECTOR('',#11555,0.7);
#3717=CIRCLE('',#9593,0.505);
#3718=CIRCLE('',#9594,0.505);
#3719=CIRCLE('',#9596,0.7);
#3720=CIRCLE('',#9597,0.7);
#4297=VERTEX_POINT('',#14602);
#4298=VERTEX_POINT('',#14604);
#4299=VERTEX_POINT('',#14608);
#4300=VERTEX_POINT('',#14610);
#5152=EDGE_CURVE('',#4297,#4297,#3717,.T.);
#5153=EDGE_CURVE('',#4297,#4298,#2733,.T.);
#5154=EDGE_CURVE('',#4298,#4298,#3718,.T.);
#5155=EDGE_CURVE('',#4299,#4299,#3719,.T.);
#5156=EDGE_CURVE('',#4299,#4300,#2734,.T.);
#5157=EDGE_CURVE('',#4300,#4300,#3720,.T.);
#6683=ORIENTED_EDGE('',*,*,#5152,.F.);
#6684=ORIENTED_EDGE('',*,*,#5153,.T.);
#6685=ORIENTED_EDGE('',*,*,#5154,.T.);
#6686=ORIENTED_EDGE('',*,*,#5153,.F.);
#6687=ORIENTED_EDGE('',*,*,#5155,.F.);
#6688=ORIENTED_EDGE('',*,*,#5156,.T.);
#6689=ORIENTED_EDGE('',*,*,#5157,.T.);
#6690=ORIENTED_EDGE('',*,*,#5156,.F.);
#6691=ORIENTED_EDGE('',*,*,#5155,.T.);
#6692=ORIENTED_EDGE('',*,*,#5152,.T.);
#6693=ORIENTED_EDGE('',*,*,#5157,.F.);
#6694=ORIENTED_EDGE('',*,*,#5154,.F.);
#7764=CYLINDRICAL_SURFACE('',#9592,0.505);
#7765=CYLINDRICAL_SURFACE('',#9595,0.7);
#8096=ADVANCED_FACE('',(#1493),#7764,.F.);
#8097=ADVANCED_FACE('',(#1494),#7765,.T.);
#8098=ADVANCED_FACE('',(#1495,#885),#1105,.T.);
#8099=ADVANCED_FACE('',(#1496,#886),#1106,.F.);
#8388=CLOSED_SHELL('',(#8096,#8097,#8098,#8099));
#9591=AXIS2_PLACEMENT_3D('',#14600,#11542,#11543);
#9592=AXIS2_PLACEMENT_3D('',#14601,#11544,#11545);
#9593=AXIS2_PLACEMENT_3D('',#14603,#11546,#11547);
#9594=AXIS2_PLACEMENT_3D('',#14606,#11549,#11550);
#9595=AXIS2_PLACEMENT_3D('',#14607,#11551,#11552);
#9596=AXIS2_PLACEMENT_3D('',#14609,#11553,#11554);
#9597=AXIS2_PLACEMENT_3D('',#14612,#11556,#11557);
#9598=AXIS2_PLACEMENT_3D('',#14613,#11558,#11559);
#9599=AXIS2_PLACEMENT_3D('',#14614,#11560,#11561);
#11542=DIRECTION('axis',(0.,0.,1.));
#11543=DIRECTION('refdir',(1.,0.,0.));
#11544=DIRECTION('center_axis',(0.,1.,0.));
#11545=DIRECTION('ref_axis',(1.,0.,0.));
#11546=DIRECTION('center_axis',(0.,-1.,0.));
#11547=DIRECTION('ref_axis',(1.,0.,0.));
#11548=DIRECTION('',(0.,-1.,0.));
#11549=DIRECTION('center_axis',(0.,-1.,0.));
#11550=DIRECTION('ref_axis',(1.,0.,0.));
#11551=DIRECTION('center_axis',(0.,1.,0.));
#11552=DIRECTION('ref_axis',(1.,0.,0.));
#11553=DIRECTION('center_axis',(0.,1.,0.));
#11554=DIRECTION('ref_axis',(1.,0.,0.));
#11555=DIRECTION('',(0.,-1.,0.));
#11556=DIRECTION('center_axis',(0.,1.,0.));
#11557=DIRECTION('ref_axis',(1.,0.,0.));
#11558=DIRECTION('center_axis',(0.,1.,0.));
#11559=DIRECTION('ref_axis',(1.,0.,0.));
#11560=DIRECTION('center_axis',(0.,1.,0.));
#11561=DIRECTION('ref_axis',(1.,0.,0.));
#14600=CARTESIAN_POINT('',(0.,0.,0.));
#14601=CARTESIAN_POINT('Origin',(0.,15.45,3.5));
#14602=CARTESIAN_POINT('',(-0.505,15.9,3.5));
#14603=CARTESIAN_POINT('Origin',(0.,15.9,3.5));
#14604=CARTESIAN_POINT('',(-0.505,15.45,3.5));
#14605=CARTESIAN_POINT('',(-0.505,15.45,3.5));
#14606=CARTESIAN_POINT('Origin',(0.,15.45,3.5));
#14607=CARTESIAN_POINT('Origin',(0.,15.45,3.5));
#14608=CARTESIAN_POINT('',(-0.7,15.9,3.5));
#14609=CARTESIAN_POINT('Origin',(0.,15.9,3.5));
#14610=CARTESIAN_POINT('',(-0.7,15.45,3.5));
#14611=CARTESIAN_POINT('',(-0.7,15.45,3.5));
#14612=CARTESIAN_POINT('Origin',(0.,15.45,3.5));
#14613=CARTESIAN_POINT('Origin',(0.,15.9,3.5));
#14614=CARTESIAN_POINT('Origin',(0.,15.45,3.5));
#16168=UNCERTAINTY_MEASURE_WITH_UNIT(LENGTH_MEASURE(0.001),#16282,
'DISTANCE_ACCURACY_VALUE',
'Maximum model space distance between geometric entities at asserted c
onnectivities');
#16212=UNCERTAINTY_MEASURE_WITH_UNIT(LENGTH_MEASURE(0.001),#16282,
'DISTANCE_ACCURACY_VALUE',
'Maximum model space distance between geometric entities at asserted c
onnectivities');
#16237=(
GEOMETRIC_REPRESENTATION_CONTEXT(3)
GLOBAL_UNCERTAINTY_ASSIGNED_CONTEXT((#16168))
GLOBAL_UNIT_ASSIGNED_CONTEXT((#16282,#16284,#16285))
REPRESENTATION_CONTEXT('','3D')
);
#16281=(
GEOMETRIC_REPRESENTATION_CONTEXT(3)
GLOBAL_UNCERTAINTY_ASSIGNED_CONTEXT((#16212))
GLOBAL_UNIT_ASSIGNED_CONTEXT((#16282,#16284,#16285))
REPRESENTATION_CONTEXT('','3D')
);
#16282=(
LENGTH_UNIT()
NAMED_UNIT(*)
SI_UNIT(.CENTI.,.METRE.)
);
#16284=(
NAMED_UNIT(*)
PLANE_ANGLE_UNIT()
SI_UNIT($,.RADIAN.)
);
#16285=(
NAMED_UNIT(*)
SI_UNIT($,.STERADIAN.)
SOLID_ANGLE_UNIT()
);
#16310=SHAPE_DEFINITION_REPRESENTATION(#16404,#16543);
#16404=PRODUCT_DEFINITION_SHAPE('',$,#16612);
#16543=SHAPE_REPRESENTATION('',(#9591),#16237);
#16587=PRODUCT_DEFINITION_CONTEXT('part definition',#16793,'design');
#16612=PRODUCT_DEFINITION('Inner race spacer (1)','Inner race spacer (1)',
#16680,#16587);
#16680=PRODUCT_DEFINITION_FORMATION('',$,#16819);
#16793=APPLICATION_CONTEXT(
'Core Data for Automotive Mechanical Design Process');
#16794=PRODUCT_CONTEXT('part definition',#16793,'mechanical');
#16819=PRODUCT('Inner race spacer (1)','Inner race spacer (1)',
'Inner race spacer (1)',(#16794));
#16926=COLOUR_RGB('Grey',0.48,0.52,0.57);
#16927=FILL_AREA_STYLE_COLOUR('',#16926);
#16928=FILL_AREA_STYLE('',(#16927));
#16929=SURFACE_STYLE_FILL_AREA(#16928);
#16930=SURFACE_SIDE_STYLE('',(#16929));
#16931=SURFACE_STYLE_USAGE(.BOTH.,#16930);
#16932=PRESENTATION_STYLE_ASSIGNMENT((#16931));
ENDSEC;
END-ISO-10303-21;
